ISO-10303-21;
HEADER;
/* Generated by software containing ST-Developer
 * from STEP Tools, Inc. (www.steptools.com) 
 */

FILE_DESCRIPTION(
/* description */ ('Timing belt drive module 2 mm Pitch Timing 20T-40T'),

/* implementation_level */ '2;1');

FILE_NAME(
/* name */ 'M4x30 mounting screw.step',
/* time_stamp */ '2026-10-28T03:25:12-07:00',
/* author */ (''),
/* organization */ (''),
/* preprocessor_version */ 'ST-DEVELOPER v20.2',
/* originating_system */ 'Autodesk Translation Framework v15.17.0.0',
/* authorisation */ '');

FILE_SCHEMA (('AUTOMOTIVE_DESIGN { 1 0 10303 214 3 1 1 }'));
ENDSEC;

DATA;
#10=MECHANICAL_DESIGN_GEOMETRIC_PRESENTATION_REPRESENTATION('',(#553),#17830);
#11=ORIENTED_CLOSED_SHELL('',*,#9010,.F.);
#14=BREP_WITH_VOIDS('Body1',#9011,(#11));
#419=CONICAL_SURFACE('',#10027,0.325,0.785398163397448);
#420=CONICAL_SURFACE('',#10031,0.335,0.785398163397448);
#421=CONICAL_SURFACE('',#10035,0.21,0.463647609000806);
#422=CONICAL_SURFACE('',#10039,0.18,0.785398163397448);
#459=SHAPE_REPRESENTATION_RELATIONSHIP('SRR','None',#18030,#502);
#502=ADVANCED_BREP_SHAPE_REPRESENTATION('',(#14),#17805);
#553=STYLED_ITEM('',(#18324),#14);
#718=FACE_BOUND('',#1790,.T.);
#719=FACE_BOUND('',#1798,.T.);
#870=PLANE('',#10011);
#871=PLANE('',#10012);
#872=PLANE('',#10013);
#873=PLANE('',#10014);
#874=PLANE('',#10015);
#875=PLANE('',#10016);
#876=PLANE('',#10017);
#877=PLANE('',#10018);
#878=PLANE('',#10019);
#879=PLANE('',#10024);
#880=PLANE('',#10025);
#881=PLANE('',#10033);
#1179=FACE_OUTER_BOUND('',#1781,.T.);
#1180=FACE_OUTER_BOUND('',#1782,.T.);
#1181=FACE_OUTER_BOUND('',#1783,.T.);
#1182=FACE_OUTER_BOUND('',#1784,.T.);
#1183=FACE_OUTER_BOUND('',#1785,.T.);
#1184=FACE_OUTER_BOUND('',#1786,.T.);
#1185=FACE_OUTER_BOUND('',#1787,.T.);
#1186=FACE_OUTER_BOUND('',#1788,.T.);
#1187=FACE_OUTER_BOUND('',#1789,.T.);
#1188=FACE_OUTER_BOUND('',#1791,.T.);
#1189=FACE_OUTER_BOUND('',#1792,.T.);
#1190=FACE_OUTER_BOUND('',#1793,.T.);
#1191=FACE_OUTER_BOUND('',#1794,.T.);
#1192=FACE_OUTER_BOUND('',#1795,.T.);
#1193=FACE_OUTER_BOUND('',#1796,.T.);
#1194=FACE_OUTER_BOUND('',#1797,.T.);
#1195=FACE_OUTER_BOUND('',#1799,.T.);
#1196=FACE_OUTER_BOUND('',#1800,.T.);
#1197=FACE_OUTER_BOUND('',#1801,.T.);
#1781=EDGE_LOOP('',(#6753,#6754,#6755,#6756));
#1782=EDGE_LOOP('',(#6757,#6758,#6759,#6760));
#1783=EDGE_LOOP('',(#6761,#6762,#6763,#6764));
#1784=EDGE_LOOP('',(#6765,#6766,#6767,#6768));
#1785=EDGE_LOOP('',(#6769,#6770,#6771,#6772));
#1786=EDGE_LOOP('',(#6773,#6774,#6775,#6776));
#1787=EDGE_LOOP('',(#6777,#6778,#6779,#6780,#6781,#6782));
#1788=EDGE_LOOP('',(#6783,#6784,#6785,#6786,#6787,#6788));
#1789=EDGE_LOOP('',(#6789));
#1790=EDGE_LOOP('',(#6790));
#1791=EDGE_LOOP('',(#6791,#6792,#6793,#6794));
#1792=EDGE_LOOP('',(#6795));
#1793=EDGE_LOOP('',(#6796));
#1794=EDGE_LOOP('',(#6797,#6798,#6799,#6800));
#1795=EDGE_LOOP('',(#6801,#6802,#6803,#6804));
#1796=EDGE_LOOP('',(#6805,#6806,#6807,#6808));
#1797=EDGE_LOOP('',(#6809));
#1798=EDGE_LOOP('',(#6810));
#1799=EDGE_LOOP('',(#6811,#6812,#6813,#6814));
#1800=EDGE_LOOP('',(#6815,#6816,#6817,#6818));
#1801=EDGE_LOOP('',(#6819,#6820,#6821,#6822));
#2388=CIRCLE('',#10020,0.2);
#2389=CIRCLE('',#10021,0.16);
#2390=CIRCLE('',#10023,0.2);
#2391=CIRCLE('',#10026,0.3);
#2392=CIRCLE('',#10028,0.35);
#2393=CIRCLE('',#10030,0.35);
#2394=CIRCLE('',#10032,0.32);
#2395=CIRCLE('',#10034,0.22);
#2396=CIRCLE('',#10036,0.1954);
#2397=CIRCLE('',#10038,0.1954);
#3014=LINE('',#15287,#3492);
#3015=LINE('',#15289,#3493);
#3016=LINE('',#15291,#3494);
#3017=LINE('',#15292,#3495);
#3018=LINE('',#15295,#3496);
#3019=LINE('',#15297,#3497);
#3020=LINE('',#15298,#3498);
#3021=LINE('',#15301,#3499);
#3022=LINE('',#15303,#3500);
#3023=LINE('',#15304,#3501);
#3024=LINE('',#15307,#3502);
#3025=LINE('',#15309,#3503);
#3026=LINE('',#15310,#3504);
#3027=LINE('',#15313,#3505);
#3028=LINE('',#15315,#3506);
#3029=LINE('',#15316,#3507);
#3030=LINE('',#15318,#3508);
#3031=LINE('',#15319,#3509);
#3032=LINE('',#15329,#3510);
#3033=LINE('',#15338,#3511);
#3034=LINE('',#15342,#3512);
#3035=LINE('',#15346,#3513);
#3036=LINE('',#15353,#3514);
#3037=LINE('',#15357,#3515);
#3038=LINE('',#15359,#3516);
#3492=VECTOR('',#12025,1.);
#3493=VECTOR('',#12026,1.);
#3494=VECTOR('',#12027,1.);
#3495=VECTOR('',#12028,1.);
#3496=VECTOR('',#12031,1.);
#3497=VECTOR('',#12032,1.);
#3498=VECTOR('',#12033,1.);
#3499=VECTOR('',#12036,1.);
#3500=VECTOR('',#12037,1.);
#3501=VECTOR('',#12038,1.);
#3502=VECTOR('',#12041,1.);
#3503=VECTOR('',#12042,1.);
#3504=VECTOR('',#12043,1.);
#3505=VECTOR('',#12046,1.);
#3506=VECTOR('',#12047,1.);
#3507=VECTOR('',#12048,1.);
#3508=VECTOR('',#12051,1.);
#3509=VECTOR('',#12052,1.);
#3510=VECTOR('',#12065,0.2);
#3511=VECTOR('',#12078,0.325);
#3512=VECTOR('',#12083,0.35);
#3513=VECTOR('',#12088,0.335);
#3514=VECTOR('',#12097,0.21);
#3515=VECTOR('',#12102,0.2);
#3516=VECTOR('',#12105,0.18);
#4082=VERTEX_POINT('',#15285);
#4083=VERTEX_POINT('',#15286);
#4084=VERTEX_POINT('',#15288);
#4085=VERTEX_POINT('',#15290);
#4086=VERTEX_POINT('',#15294);
#4087=VERTEX_POINT('',#15296);
#4088=VERTEX_POINT('',#15300);
#4089=VERTEX_POINT('',#15302);
#4090=VERTEX_POINT('',#15306);
#4091=VERTEX_POINT('',#15308);
#4092=VERTEX_POINT('',#15312);
#4093=VERTEX_POINT('',#15314);
#4094=VERTEX_POINT('',#15323);
#4095=VERTEX_POINT('',#15325);
#4096=VERTEX_POINT('',#15328);
#4097=VERTEX_POINT('',#15333);
#4098=VERTEX_POINT('',#15336);
#4099=VERTEX_POINT('',#15340);
#4100=VERTEX_POINT('',#15344);
#4101=VERTEX_POINT('',#15348);
#4102=VERTEX_POINT('',#15351);
#4103=VERTEX_POINT('',#15355);
#5059=EDGE_CURVE('',#4082,#4083,#3014,.T.);
#5060=EDGE_CURVE('',#4083,#4084,#3015,.T.);
#5061=EDGE_CURVE('',#4084,#4085,#3016,.T.);
#5062=EDGE_CURVE('',#4082,#4085,#3017,.T.);
#5063=EDGE_CURVE('',#4083,#4086,#3018,.T.);
#5064=EDGE_CURVE('',#4086,#4087,#3019,.T.);
#5065=EDGE_CURVE('',#4087,#4084,#3020,.T.);
#5066=EDGE_CURVE('',#4086,#4088,#3021,.T.);
#5067=EDGE_CURVE('',#4088,#4089,#3022,.T.);
#5068=EDGE_CURVE('',#4089,#4087,#3023,.T.);
#5069=EDGE_CURVE('',#4088,#4090,#3024,.T.);
#5070=EDGE_CURVE('',#4090,#4091,#3025,.T.);
#5071=EDGE_CURVE('',#4091,#4089,#3026,.T.);
#5072=EDGE_CURVE('',#4090,#4092,#3027,.T.);
#5073=EDGE_CURVE('',#4092,#4093,#3028,.T.);
#5074=EDGE_CURVE('',#4093,#4091,#3029,.T.);
#5075=EDGE_CURVE('',#4092,#4082,#3030,.T.);
#5076=EDGE_CURVE('',#4085,#4093,#3031,.T.);
#5077=EDGE_CURVE('',#4094,#4094,#2388,.T.);
#5078=EDGE_CURVE('',#4095,#4095,#2389,.T.);
#5079=EDGE_CURVE('',#4094,#4096,#3032,.T.);
#5080=EDGE_CURVE('',#4096,#4096,#2390,.T.);
#5081=EDGE_CURVE('',#4097,#4097,#2391,.T.);
#5082=EDGE_CURVE('',#4098,#4098,#2392,.T.);
#5083=EDGE_CURVE('',#4098,#4097,#3033,.T.);
#5084=EDGE_CURVE('',#4099,#4099,#2393,.T.);
#5085=EDGE_CURVE('',#4099,#4098,#3034,.T.);
#5086=EDGE_CURVE('',#4100,#4100,#2394,.T.);
#5087=EDGE_CURVE('',#4100,#4099,#3035,.T.);
#5088=EDGE_CURVE('',#4101,#4101,#2395,.T.);
#5089=EDGE_CURVE('',#4102,#4102,#2396,.F.);
#5090=EDGE_CURVE('',#4102,#4101,#3036,.T.);
#5091=EDGE_CURVE('',#4103,#4103,#2397,.F.);
#5092=EDGE_CURVE('',#4103,#4102,#3037,.T.);
#5093=EDGE_CURVE('',#4095,#4103,#3038,.T.);
#6753=ORIENTED_EDGE('',*,*,#5059,.T.);
#6754=ORIENTED_EDGE('',*,*,#5060,.T.);
#6755=ORIENTED_EDGE('',*,*,#5061,.T.);
#6756=ORIENTED_EDGE('',*,*,#5062,.F.);
#6757=ORIENTED_EDGE('',*,*,#5063,.T.);
#6758=ORIENTED_EDGE('',*,*,#5064,.T.);
#6759=ORIENTED_EDGE('',*,*,#5065,.T.);
#6760=ORIENTED_EDGE('',*,*,#5060,.F.);
#6761=ORIENTED_EDGE('',*,*,#5066,.T.);
#6762=ORIENTED_EDGE('',*,*,#5067,.T.);
#6763=ORIENTED_EDGE('',*,*,#5068,.T.);
#6764=ORIENTED_EDGE('',*,*,#5064,.F.);
#6765=ORIENTED_EDGE('',*,*,#5069,.T.);
#6766=ORIENTED_EDGE('',*,*,#5070,.T.);
#6767=ORIENTED_EDGE('',*,*,#5071,.T.);
#6768=ORIENTED_EDGE('',*,*,#5067,.F.);
#6769=ORIENTED_EDGE('',*,*,#5072,.T.);
#6770=ORIENTED_EDGE('',*,*,#5073,.T.);
#6771=ORIENTED_EDGE('',*,*,#5074,.T.);
#6772=ORIENTED_EDGE('',*,*,#5070,.F.);
#6773=ORIENTED_EDGE('',*,*,#5075,.T.);
#6774=ORIENTED_EDGE('',*,*,#5062,.T.);
#6775=ORIENTED_EDGE('',*,*,#5076,.T.);
#6776=ORIENTED_EDGE('',*,*,#5073,.F.);
#6777=ORIENTED_EDGE('',*,*,#5075,.F.);
#6778=ORIENTED_EDGE('',*,*,#5072,.F.);
#6779=ORIENTED_EDGE('',*,*,#5069,.F.);
#6780=ORIENTED_EDGE('',*,*,#5066,.F.);
#6781=ORIENTED_EDGE('',*,*,#5063,.F.);
#6782=ORIENTED_EDGE('',*,*,#5059,.F.);
#6783=ORIENTED_EDGE('',*,*,#5076,.F.);
#6784=ORIENTED_EDGE('',*,*,#5061,.F.);
#6785=ORIENTED_EDGE('',*,*,#5065,.F.);
#6786=ORIENTED_EDGE('',*,*,#5068,.F.);
#6787=ORIENTED_EDGE('',*,*,#5071,.F.);
#6788=ORIENTED_EDGE('',*,*,#5074,.F.);
#6789=ORIENTED_EDGE('',*,*,#5077,.T.);
#6790=ORIENTED_EDGE('',*,*,#5078,.T.);
#6791=ORIENTED_EDGE('',*,*,#5077,.F.);
#6792=ORIENTED_EDGE('',*,*,#5079,.T.);
#6793=ORIENTED_EDGE('',*,*,#5080,.T.);
#6794=ORIENTED_EDGE('',*,*,#5079,.F.);
#6795=ORIENTED_EDGE('',*,*,#5080,.F.);
#6796=ORIENTED_EDGE('',*,*,#5081,.F.);
#6797=ORIENTED_EDGE('',*,*,#5082,.F.);
#6798=ORIENTED_EDGE('',*,*,#5083,.T.);
#6799=ORIENTED_EDGE('',*,*,#5081,.T.);
#6800=ORIENTED_EDGE('',*,*,#5083,.F.);
#6801=ORIENTED_EDGE('',*,*,#5084,.F.);
#6802=ORIENTED_EDGE('',*,*,#5085,.T.);
#6803=ORIENTED_EDGE('',*,*,#5082,.T.);
#6804=ORIENTED_EDGE('',*,*,#5085,.F.);
#6805=ORIENTED_EDGE('',*,*,#5086,.F.);
#6806=ORIENTED_EDGE('',*,*,#5087,.T.);
#6807=ORIENTED_EDGE('',*,*,#5084,.T.);
#6808=ORIENTED_EDGE('',*,*,#5087,.F.);
#6809=ORIENTED_EDGE('',*,*,#5086,.T.);
#6810=ORIENTED_EDGE('',*,*,#5088,.F.);
#6811=ORIENTED_EDGE('',*,*,#5089,.F.);
#6812=ORIENTED_EDGE('',*,*,#5090,.T.);
#6813=ORIENTED_EDGE('',*,*,#5088,.T.);
#6814=ORIENTED_EDGE('',*,*,#5090,.F.);
#6815=ORIENTED_EDGE('',*,*,#5091,.F.);
#6816=ORIENTED_EDGE('',*,*,#5092,.T.);
#6817=ORIENTED_EDGE('',*,*,#5089,.T.);
#6818=ORIENTED_EDGE('',*,*,#5092,.F.);
#6819=ORIENTED_EDGE('',*,*,#5078,.F.);
#6820=ORIENTED_EDGE('',*,*,#5093,.T.);
#6821=ORIENTED_EDGE('',*,*,#5091,.T.);
#6822=ORIENTED_EDGE('',*,*,#5093,.F.);
#8279=CYLINDRICAL_SURFACE('',#10022,0.2);
#8280=CYLINDRICAL_SURFACE('',#10029,0.35);
#8281=CYLINDRICAL_SURFACE('',#10037,0.1954);
#8677=ADVANCED_FACE('',(#1179),#870,.F.);
#8678=ADVANCED_FACE('',(#1180),#871,.F.);
#8679=ADVANCED_FACE('',(#1181),#872,.F.);
#8680=ADVANCED_FACE('',(#1182),#873,.F.);
#8681=ADVANCED_FACE('',(#1183),#874,.F.);
#8682=ADVANCED_FACE('',(#1184),#875,.F.);
#8683=ADVANCED_FACE('',(#1185),#876,.F.);
#8684=ADVANCED_FACE('',(#1186),#877,.F.);
#8685=ADVANCED_FACE('',(#1187,#718),#878,.T.);
#8686=ADVANCED_FACE('',(#1188),#8279,.T.);
#8687=ADVANCED_FACE('',(#1189),#879,.F.);
#8688=ADVANCED_FACE('',(#1190),#880,.T.);
#8689=ADVANCED_FACE('',(#1191),#419,.T.);
#8690=ADVANCED_FACE('',(#1192),#8280,.T.);
#8691=ADVANCED_FACE('',(#1193),#420,.T.);
#8692=ADVANCED_FACE('',(#1194,#719),#881,.T.);
#8693=ADVANCED_FACE('',(#1195),#421,.T.);
#8694=ADVANCED_FACE('',(#1196),#8281,.T.);
#8695=ADVANCED_FACE('',(#1197),#422,.T.);
#9010=CLOSED_SHELL('',(#8677,#8678,#8679,#8680,#8681,#8682,#8683,#8684));
#9011=CLOSED_SHELL('',(#8685,#8686,#8687,#8688,#8689,#8690,#8691,#8692,
#8693,#8694,#8695));
#10010=AXIS2_PLACEMENT_3D('',#15283,#12021,#12022);
#10011=AXIS2_PLACEMENT_3D('',#15284,#12023,#12024);
#10012=AXIS2_PLACEMENT_3D('',#15293,#12029,#12030);
#10013=AXIS2_PLACEMENT_3D('',#15299,#12034,#12035);
#10014=AXIS2_PLACEMENT_3D('',#15305,#12039,#12040);
#10015=AXIS2_PLACEMENT_3D('',#15311,#12044,#12045);
#10016=AXIS2_PLACEMENT_3D('',#15317,#12049,#12050);
#10017=AXIS2_PLACEMENT_3D('',#15320,#12053,#12054);
#10018=AXIS2_PLACEMENT_3D('',#15321,#12055,#12056);
#10019=AXIS2_PLACEMENT_3D('',#15322,#12057,#12058);
#10020=AXIS2_PLACEMENT_3D('',#15324,#12059,#12060);
#10021=AXIS2_PLACEMENT_3D('',#15326,#12061,#12062);
#10022=AXIS2_PLACEMENT_3D('',#15327,#12063,#12064);
#10023=AXIS2_PLACEMENT_3D('',#15330,#12066,#12067);
#10024=AXIS2_PLACEMENT_3D('',#15331,#12068,#12069);
#10025=AXIS2_PLACEMENT_3D('',#15332,#12070,#12071);
#10026=AXIS2_PLACEMENT_3D('',#15334,#12072,#12073);
#10027=AXIS2_PLACEMENT_3D('',#15335,#12074,#12075);
#10028=AXIS2_PLACEMENT_3D('',#15337,#12076,#12077);
#10029=AXIS2_PLACEMENT_3D('',#15339,#12079,#12080);
#10030=AXIS2_PLACEMENT_3D('',#15341,#12081,#12082);
#10031=AXIS2_PLACEMENT_3D('',#15343,#12084,#12085);
#10032=AXIS2_PLACEMENT_3D('',#15345,#12086,#12087);
#10033=AXIS2_PLACEMENT_3D('',#15347,#12089,#12090);
#10034=AXIS2_PLACEMENT_3D('',#15349,#12091,#12092);
#10035=AXIS2_PLACEMENT_3D('',#15350,#12093,#12094);
#10036=AXIS2_PLACEMENT_3D('',#15352,#12095,#12096);
#10037=AXIS2_PLACEMENT_3D('',#15354,#12098,#12099);
#10038=AXIS2_PLACEMENT_3D('',#15356,#12100,#12101);
#10039=AXIS2_PLACEMENT_3D('',#15358,#12103,#12104);
#12021=DIRECTION('axis',(0.,0.,1.));
#12022=DIRECTION('refdir',(1.,0.,0.));
#12023=DIRECTION('center_axis',(0.866025403784439,0.,-0.5));
#12024=DIRECTION('ref_axis',(0.5,0.,0.866025403784439));
#12025=DIRECTION('',(-0.5,0.,-0.866025403784439));
#12026=DIRECTION('',(0.,-1.,0.));
#12027=DIRECTION('',(0.5,0.,0.866025403784439));
#12028=DIRECTION('',(0.,-1.,0.));
#12029=DIRECTION('center_axis',(1.60246890531964E-16,0.,-1.));
#12030=DIRECTION('ref_axis',(1.,0.,1.60246890531964E-16));
#12031=DIRECTION('',(-1.,0.,-1.60246890531964E-16));
#12032=DIRECTION('',(0.,-1.,0.));
#12033=DIRECTION('',(1.,0.,1.60246890531964E-16));
#12034=DIRECTION('center_axis',(-0.866025403784439,0.,-0.5));
#12035=DIRECTION('ref_axis',(0.5,0.,-0.866025403784439));
#12036=DIRECTION('',(-0.5,0.,0.866025403784439));
#12037=DIRECTION('',(0.,-1.,0.));
#12038=DIRECTION('',(0.5,0.,-0.866025403784439));
#12039=DIRECTION('center_axis',(-0.866025403784439,0.,0.5));
#12040=DIRECTION('ref_axis',(-0.5,0.,-0.866025403784439));
#12041=DIRECTION('',(0.5,0.,0.866025403784439));
#12042=DIRECTION('',(0.,-1.,0.));
#12043=DIRECTION('',(-0.5,0.,-0.866025403784439));
#12044=DIRECTION('center_axis',(-1.60246890531964E-16,0.,1.));
#12045=DIRECTION('ref_axis',(-1.,0.,-1.60246890531964E-16));
#12046=DIRECTION('',(1.,0.,1.60246890531964E-16));
#12047=DIRECTION('',(0.,-1.,0.));
#12048=DIRECTION('',(-1.,0.,-1.60246890531964E-16));
#12049=DIRECTION('center_axis',(0.866025403784439,0.,0.5));
#12050=DIRECTION('ref_axis',(-0.5,0.,0.866025403784439));
#12051=DIRECTION('',(0.5,0.,-0.866025403784439));
#12052=DIRECTION('',(-0.5,0.,0.866025403784439));
#12053=DIRECTION('center_axis',(0.,1.,0.));
#12054=DIRECTION('ref_axis',(1.,0.,0.));
#12055=DIRECTION('center_axis',(0.,-1.,0.));
#12056=DIRECTION('ref_axis',(0.,0.,-1.));
#12057=DIRECTION('center_axis',(0.,1.,0.));
#12058=DIRECTION('ref_axis',(1.,0.,0.));
#12059=DIRECTION('center_axis',(0.,1.,0.));
#12060=DIRECTION('ref_axis',(1.,0.,0.));
#12061=DIRECTION('center_axis',(0.,-1.,0.));
#12062=DIRECTION('ref_axis',(1.,0.,0.));
#12063=DIRECTION('center_axis',(0.,1.,0.));
#12064=DIRECTION('ref_axis',(1.,0.,0.));
#12065=DIRECTION('',(0.,-1.,0.));
#12066=DIRECTION('center_axis',(0.,1.,0.));
#12067=DIRECTION('ref_axis',(1.,0.,0.));
#12068=DIRECTION('center_axis',(0.,1.,0.));
#12069=DIRECTION('ref_axis',(1.,0.,0.));
#12070=DIRECTION('center_axis',(0.,1.,0.));
#12071=DIRECTION('ref_axis',(0.,0.,1.));
#12072=DIRECTION('center_axis',(0.,-1.,0.));
#12073=DIRECTION('ref_axis',(1.,0.,0.));
#12074=DIRECTION('center_axis',(0.,-1.,0.));
#12075=DIRECTION('ref_axis',(1.,0.,0.));
#12076=DIRECTION('center_axis',(0.,-1.,0.));
#12077=DIRECTION('ref_axis',(1.,0.,0.));
#12078=DIRECTION('',(0.707106781186547,0.707106781186548,8.65956056235493E-17));
#12079=DIRECTION('center_axis',(0.,-1.,0.));
#12080=DIRECTION('ref_axis',(1.,0.,0.));
#12081=DIRECTION('center_axis',(0.,-1.,0.));
#12082=DIRECTION('ref_axis',(1.,0.,0.));
#12083=DIRECTION('',(0.,1.,0.));
#12084=DIRECTION('center_axis',(0.,1.,0.));
#12085=DIRECTION('ref_axis',(1.,0.,0.));
#12086=DIRECTION('center_axis',(0.,-1.,0.));
#12087=DIRECTION('ref_axis',(1.,0.,0.));
#12088=DIRECTION('',(-0.707106781186547,0.707106781186548,-8.65956056235493E-17));
#12089=DIRECTION('center_axis',(0.,-1.,0.));
#12090=DIRECTION('ref_axis',(0.,0.,-1.));
#12091=DIRECTION('center_axis',(0.,-1.,0.));
#12092=DIRECTION('ref_axis',(1.,0.,0.));
#12093=DIRECTION('center_axis',(0.,1.,0.));
#12094=DIRECTION('ref_axis',(1.,0.,0.));
#12095=DIRECTION('center_axis',(0.,1.,0.));
#12096=DIRECTION('ref_axis',(1.,0.,0.));
#12097=DIRECTION('',(-0.447213595499958,0.894427190999916,-5.47678698264203E-17));
#12098=DIRECTION('center_axis',(0.,-1.,0.));
#12099=DIRECTION('ref_axis',(1.,0.,0.));
#12100=DIRECTION('center_axis',(0.,1.,0.));
#12101=DIRECTION('ref_axis',(1.,0.,0.));
#12102=DIRECTION('',(0.,1.,0.));
#12103=DIRECTION('center_axis',(0.,1.,0.));
#12104=DIRECTION('ref_axis',(1.,0.,0.));
#12105=DIRECTION('',(-0.707106781186547,0.707106781186548,-8.65956056235493E-17));
#15283=CARTESIAN_POINT('',(0.,0.,0.));
#15284=CARTESIAN_POINT('Origin',(0.0866025403784439,-0.4,-0.15));
#15285=CARTESIAN_POINT('',(0.173205080756888,-0.4,0.));
#15286=CARTESIAN_POINT('',(0.0866025403784439,-0.4,-0.15));
#15287=CARTESIAN_POINT('',(0.173205080756888,-0.4,0.));
#15288=CARTESIAN_POINT('',(0.0866025403784439,-0.64,-0.15));
#15289=CARTESIAN_POINT('',(0.0866025403784439,-0.4,-0.15));
#15290=CARTESIAN_POINT('',(0.173205080756888,-0.64,0.));
#15291=CARTESIAN_POINT('',(0.173205080756888,-0.64,0.));
#15292=CARTESIAN_POINT('',(0.173205080756888,-0.4,0.));
#15293=CARTESIAN_POINT('Origin',(-0.0866025403784438,-0.4,-0.15));
#15294=CARTESIAN_POINT('',(-0.0866025403784438,-0.4,-0.15));
#15295=CARTESIAN_POINT('',(0.0866025403784439,-0.4,-0.15));
#15296=CARTESIAN_POINT('',(-0.0866025403784438,-0.64,-0.15));
#15297=CARTESIAN_POINT('',(-0.0866025403784438,-0.4,-0.15));
#15298=CARTESIAN_POINT('',(0.0866025403784439,-0.64,-0.15));
#15299=CARTESIAN_POINT('Origin',(-0.173205080756888,-0.4,-2.77555756156289E-17));
#15300=CARTESIAN_POINT('',(-0.173205080756888,-0.4,-2.12115047744981E-17));
#15301=CARTESIAN_POINT('',(-0.0866025403784438,-0.4,-0.15));
#15302=CARTESIAN_POINT('',(-0.173205080756888,-0.64,-2.77555756156289E-17));
#15303=CARTESIAN_POINT('',(-0.173205080756888,-0.4,-2.12115047744981E-17));
#15304=CARTESIAN_POINT('',(-0.0866025403784438,-0.64,-0.15));
#15305=CARTESIAN_POINT('Origin',(-0.0866025403784439,-0.4,0.15));
#15306=CARTESIAN_POINT('',(-0.0866025403784439,-0.4,0.15));
#15307=CARTESIAN_POINT('',(-0.173205080756888,-0.4,-2.12115047744981E-17));
#15308=CARTESIAN_POINT('',(-0.0866025403784439,-0.64,0.15));
#15309=CARTESIAN_POINT('',(-0.0866025403784439,-0.4,0.15));
#15310=CARTESIAN_POINT('',(-0.173205080756888,-0.64,-2.12115047744981E-17));
#15311=CARTESIAN_POINT('Origin',(0.0866025403784439,-0.4,0.15));
#15312=CARTESIAN_POINT('',(0.0866025403784439,-0.4,0.15));
#15313=CARTESIAN_POINT('',(-0.0866025403784439,-0.4,0.15));
#15314=CARTESIAN_POINT('',(0.0866025403784439,-0.64,0.15));
#15315=CARTESIAN_POINT('',(0.0866025403784439,-0.4,0.15));
#15316=CARTESIAN_POINT('',(-0.0866025403784439,-0.64,0.15));
#15317=CARTESIAN_POINT('Origin',(0.173205080756888,-0.4,0.));
#15318=CARTESIAN_POINT('',(0.0866025403784439,-0.4,0.15));
#15319=CARTESIAN_POINT('',(0.0866025403784439,-0.64,0.15));
#15320=CARTESIAN_POINT('Origin',(0.,-0.4,-2.77555756156289E-17));
#15321=CARTESIAN_POINT('Origin',(0.,-0.64,-2.77555756156289E-17));
#15322=CARTESIAN_POINT('Origin',(0.,-1.6,0.));
#15323=CARTESIAN_POINT('',(-0.2,-1.6,2.44929359829471E-17));
#15324=CARTESIAN_POINT('Origin',(0.,-1.6,0.));
#15325=CARTESIAN_POINT('',(-0.16,-1.6,-1.95943487863577E-17));
#15326=CARTESIAN_POINT('Origin',(0.,-1.6,0.));
#15327=CARTESIAN_POINT('Origin',(0.,-3.,0.));
#15328=CARTESIAN_POINT('',(-0.2,-3.,2.44929359829471E-17));
#15329=CARTESIAN_POINT('',(-0.2,-3.,2.44929359829471E-17));
#15330=CARTESIAN_POINT('Origin',(0.,-3.,0.));
#15331=CARTESIAN_POINT('Origin',(0.,-3.,0.));
#15332=CARTESIAN_POINT('Origin',(0.3,0.4,0.));
#15333=CARTESIAN_POINT('',(-0.3,0.4,-3.67394039744206E-17));
#15334=CARTESIAN_POINT('Origin',(0.,0.4,0.));
#15335=CARTESIAN_POINT('Origin',(0.,0.375,0.));
#15336=CARTESIAN_POINT('',(-0.35,0.35,-4.28626379701573E-17));
#15337=CARTESIAN_POINT('Origin',(0.,0.35,0.));
#15338=CARTESIAN_POINT('',(-0.325,0.375,-3.9801020972289E-17));
#15339=CARTESIAN_POINT('Origin',(0.,0.19,0.));
#15340=CARTESIAN_POINT('',(-0.35,0.03,-4.28626379701574E-17));
#15341=CARTESIAN_POINT('Origin',(0.,0.03,0.));
#15342=CARTESIAN_POINT('',(-0.35,0.19,-4.28626379701574E-17));
#15343=CARTESIAN_POINT('Origin',(0.,0.0149999999999999,0.));
#15344=CARTESIAN_POINT('',(-0.32,-3.29597460435593E-17,-3.91886975727153E-17));
#15345=CARTESIAN_POINT('Origin',(0.,0.,0.));
#15346=CARTESIAN_POINT('',(-0.335,0.0149999999999999,-4.10256677714363E-17));
#15347=CARTESIAN_POINT('Origin',(0.22,0.,0.));
#15348=CARTESIAN_POINT('',(-0.22,-6.93889390390723E-18,-2.69422295812418E-17));
#15349=CARTESIAN_POINT('Origin',(0.,0.,0.));
#15350=CARTESIAN_POINT('Origin',(0.,-0.02,0.));
#15351=CARTESIAN_POINT('',(-0.1954,-0.0492,2.39295984553393E-17));
#15352=CARTESIAN_POINT('Origin',(0.,-0.0492,0.));
#15353=CARTESIAN_POINT('',(-0.21,-0.02,-2.57175827820944E-17));
#15354=CARTESIAN_POINT('Origin',(0.,-0.8,0.));
#15355=CARTESIAN_POINT('',(-0.1954,-1.5646,2.39295984553393E-17));
#15356=CARTESIAN_POINT('Origin',(0.,-1.5646,0.));
#15357=CARTESIAN_POINT('',(-0.1954,-0.8,-2.39295984553393E-17));
#15358=CARTESIAN_POINT('Origin',(0.,-1.58,0.));
#15359=CARTESIAN_POINT('',(-0.18,-1.58,-2.20436423846524E-17));
#17755=UNCERTAINTY_MEASURE_WITH_UNIT(LENGTH_MEASURE(0.001),#17831,
'DISTANCE_ACCURACY_VALUE',
'Maximum model space distance between geometric entities at asserted c
onnectivities');
#17780=UNCERTAINTY_MEASURE_WITH_UNIT(LENGTH_MEASURE(0.001),#17831,
'DISTANCE_ACCURACY_VALUE',
'Maximum model space distance between geometric entities at asserted c
onnectivities');
#17805=(
GEOMETRIC_REPRESENTATION_CONTEXT(3)
GLOBAL_UNCERTAINTY_ASSIGNED_CONTEXT((#17755))
GLOBAL_UNIT_ASSIGNED_CONTEXT((#17831,#17833,#17834))
REPRESENTATION_CONTEXT('','3D')
);
#17830=(
GEOMETRIC_REPRESENTATION_CONTEXT(3)
GLOBAL_UNCERTAINTY_ASSIGNED_CONTEXT((#17780))
GLOBAL_UNIT_ASSIGNED_CONTEXT((#17831,#17833,#17834))
REPRESENTATION_CONTEXT('','3D')
);
#17831=(
LENGTH_UNIT()
NAMED_UNIT(*)
SI_UNIT(.CENTI.,.METRE.)
);
#17833=(
NAMED_UNIT(*)
PLANE_ANGLE_UNIT()
SI_UNIT($,.RADIAN.)
);
#17834=(
NAMED_UNIT(*)
SI_UNIT($,.STERADIAN.)
SOLID_ANGLE_UNIT()
);
#17859=SHAPE_DEFINITION_REPRESENTATION(#17913,#18030);
#17913=PRODUCT_DEFINITION_SHAPE('',$,#18080);
#18030=SHAPE_REPRESENTATION('',(#10010),#17805);
#18055=PRODUCT_DEFINITION_CONTEXT('part definition',#18204,'design');
#18080=PRODUCT_DEFINITION('M4x30 mounting screw','M4x30 mounting screw',
#18129,#18055);
#18129=PRODUCT_DEFINITION_FORMATION('',$,#18230);
#18204=APPLICATION_CONTEXT(
'Core Data for Automotive Mechanical Design Process');
#18205=PRODUCT_CONTEXT('part definition',#18204,'mechanical');
#18230=PRODUCT('M4x30 mounting screw','M4x30 mounting screw',
'M4x30 mounting screw',(#18205));
#18318=COLOUR_RGB('Black',0.12,0.14,0.17);
#18319=FILL_AREA_STYLE_COLOUR('',#18318);
#18320=FILL_AREA_STYLE('',(#18319));
#18321=SURFACE_STYLE_FILL_AREA(#18320);
#18322=SURFACE_SIDE_STYLE('',(#18321));
#18323=SURFACE_STYLE_USAGE(.BOTH.,#18322);
#18324=PRESENTATION_STYLE_ASSIGNMENT((#18323));
ENDSEC;
END-ISO-10303-21;
